ISO-10303-21;
HEADER;
FILE_DESCRIPTION (('STEP AP214'),
    '1' );
FILE_NAME ('socket button head screw_iso_ISO 7380 - M5 x 25 - 25N.step',
    '2026-09-24T10:26:00',
    ( '' ),
    ( '' ),
    'SwSTEP 2.0',
    'SolidWorks 2026',
    '' );
FILE_SCHEMA (( 'AUTOMOTIVE_DESIGN' ));
ENDSEC;

DATA;
#12=DIRECTION ( 'NONE',  ( -1.000000000000000000, 0.000000000000000000, 0.000000000000000000 ) ) ;
#15=VECTOR ( 'NONE', #13017, 1000.000000000000114 ) ;
#18=DIRECTION ( 'NONE',  ( 0.000000000000000000, -1.000000000000000000, 0.000000000000000000 ) ) ;
#21=AXIS2_PLACEMENT_3D ( 'NONE', #11051, #3233, #13332 ) ;
#24=COLOUR_RGB ( '', 0.66274510, 0.83137255, 0.94901961) ;
#52=DIRECTION ( 'NONE',  ( 0.000000000000000000, 0.000000000000000000, -1.000000000000000000 ) ) ;
#56=ORIENTED_EDGE ( 'NONE', *, *, #8567, .F. ) ;
#61=CARTESIAN_POINT ( 'NONE',  ( 0.000000000000000000, -0.8660254037844428154, 1.500000000000001332 ) ) ;
#86=AXIS2_PLACEMENT_3D ( 'NONE', #5868, #6092, #4935 ) ;
#110=ORIENTED_EDGE ( 'NONE', *, *, #1310, .T. ) ;
#125=EDGE_CURVE ( 'NONE', #5215, #588, #8984, .T. ) ;
#143=ORIENTED_EDGE ( 'NONE', *, *, #10591, .T. ) ;
#167=CARTESIAN_POINT ( 'NONE',  ( 0.000000000000000000, 0.000000000000000000, 0.000000000000000000 ) ) ;
#168=CONICAL_SURFACE ( 'NONE', #12822, 1732.050807568857181, 1.047197551196592746 ) ;
#189=EDGE_LOOP ( 'NONE', ( #816, #9707, #13523, #12144 ) ) ;
#202=PLANE ( 'NONE',  #7722 ) ;
#227=AXIS2_PLACEMENT_3D ( 'NONE', #3286, #6852, #12205 ) ;
#267=ORIENTED_EDGE ( 'NONE', *, *, #8811, .F. ) ;
#281=FACE_OUTER_BOUND ( 'NONE', #2970, .T. ) ;
#283=EDGE_CURVE ( 'NONE', #3285, #4147, #432, .T. ) ;
#306=EDGE_LOOP ( 'NONE', ( #9617, #6629, #11279, #5233, #2336 ) ) ;
#324=PLANE ( 'NONE',  #4421 ) ;
#353=PLANE ( 'NONE',  #1336 ) ;
#374=AXIS2_PLACEMENT_3D ( 'NONE', #6234, #5287, #14092 ) ;
#375=VERTEX_POINT ( 'NONE', #14335 ) ;
#383=ORIENTED_EDGE ( 'NONE', *, *, #7969, .F. ) ;
#389=CARTESIAN_POINT ( 'NONE',  ( 1.560000000000005826, 0.8660254037844428154, 1.500000000000001332 ) ) ;
#400=ORIENTED_EDGE ( 'NONE', *, *, #1107, .F. ) ;
#421=DIRECTION ( 'NONE',  ( 0.000000000000000000, 1.000000000000000000, 1.224646799147353207E-16 ) ) ;
#432=LINE ( 'NONE', #11691, #9898 ) ;
#455=( NAMED_UNIT ( * ) PLANE_ANGLE_UNIT ( ) SI_UNIT ( $, .RADIAN. ) );
#514=LINE ( 'NONE', #5974, #2322 ) ;
#534=( NAMED_UNIT ( * ) SI_UNIT ( $, .STERADIAN. ) SOLID_ANGLE_UNIT ( ) );
#542=LINE ( 'NONE', #11735, #3309 ) ;
#569=CARTESIAN_POINT ( 'NONE',  ( 2.949999999999994404, 0.000000000000000000, 0.000000000000000000 ) ) ;
#579=CARTESIAN_POINT ( 'NONE',  ( 1.560000000000005826, -1.732050807568885631, 0.000000000000000000 ) ) ;
#586=ORIENTED_EDGE ( 'NONE', *, *, #1107, .T. ) ;
#588=VERTEX_POINT ( 'NONE', #1353 ) ;
#598=CARTESIAN_POINT ( 'NONE',  ( 1.560000000000005826, 0.000000000000000000, 0.000000000000000000 ) ) ;
#611=SURFACE_STYLE_USAGE ( .BOTH. , #8196 ) ;
#642=EDGE_LOOP ( 'NONE', ( #3590, #6083 ) ) ;
#647=LINE ( 'NONE', #4099, #15 ) ;
#653=CARTESIAN_POINT ( 'NONE',  ( 0.000000000000000000, 2.375000000000000000, 0.000000000000000000 ) ) ;
#658=VERTEX_POINT ( 'NONE', #8455 ) ;
#702=ADVANCED_FACE ( 'NONE', ( #11758 ), #12020, .F. ) ;
#709=LINE ( 'NONE', #5166, #6863 ) ;
#769=DIRECTION ( 'NONE',  ( 0.000000000000000000, 1.000000000000000000, 0.000000000000000000 ) ) ;
#773=EDGE_CURVE ( 'NONE', #12337, #11431, #4564, .T. ) ;
#816=ORIENTED_EDGE ( 'NONE', *, *, #12022, .T. ) ;
#819=FACE_OUTER_BOUND ( 'NONE', #5661, .T. ) ;
#823=DIRECTION ( 'NONE',  ( 0.000000000000000000, 0.000000000000000000, 1.000000000000000000 ) ) ;
#824=EDGE_CURVE ( 'NONE', #13213, #1861, #709, .T. ) ;
#837=EDGE_LOOP ( 'NONE', ( #14035, #12060, #7741 ) ) ;
#856=ORIENTED_EDGE ( 'NONE', *, *, #10678, .F. ) ;
#916=DIRECTION ( 'NONE',  ( 0.000000000000000000, 0.000000000000000000, 1.000000000000000000 ) ) ;
#930=DIRECTION ( 'NONE',  ( 1.000000000000000000, 0.000000000000000000, 0.000000000000000000 ) ) ;
#934=CIRCLE ( 'NONE', #1890, 1.500000000000000000 ) ;
#946=DIRECTION ( 'NONE',  ( -1.000000000000000000, 0.000000000000000000, 0.000000000000000000 ) ) ;
#955=PLANE ( 'NONE',  #5428 ) ;
#962=AXIS2_PLACEMENT_3D ( 'NONE', #10682, #11855, #12069 ) ;
#964=CARTESIAN_POINT ( 'NONE',  ( -997.5739745962155212, 0.000000000000000000, 0.000000000000000000 ) ) ;
#984=DIRECTION ( 'NONE',  ( 0.000000000000000000, 0.000000000000000000, 1.000000000000000000 ) ) ;
#1003=ORIENTED_EDGE ( 'NONE', *, *, #13048, .F. ) ;
#1028=DIRECTION ( 'NONE',  ( 0.000000000000000000, 0.5000000000000011102, -0.8660254037844379305 ) ) ;
#1099=DIRECTION ( 'NONE',  ( 0.000000000000000000, -1.000000000000000000, 0.000000000000000000 ) ) ;
#1101=EDGE_CURVE ( 'NONE', #2724, #13213, #13719, .T. ) ;
#1106=CARTESIAN_POINT ( 'NONE',  ( 1.560000000000005826, -1.732050807568885631, 0.000000000000000000 ) ) ;
#1107=EDGE_CURVE ( 'NONE', #588, #1326, #542, .T. ) ;
#1167=CARTESIAN_POINT ( 'NONE',  ( 1.560000000000005826, -0.8660254037844428154, 1.500000000000001332 ) ) ;
#1181=VERTEX_POINT ( 'NONE', #11809 ) ;
#1192=ORIENTED_EDGE ( 'NONE', *, *, #2488, .F. ) ;
#1209=DIRECTION ( 'NONE',  ( 0.000000000000000000, 0.000000000000000000, 1.000000000000000000 ) ) ;
#1211=VECTOR ( 'NONE', #13443, 1000.000000000000000 ) ;
#1233=CARTESIAN_POINT ( 'NONE',  ( 0.000000000000000000, 0.000000000000000000, 0.000000000000000000 ) ) ;
#1283=CARTESIAN_POINT ( 'NONE',  ( 1.560000000000005826, 0.8660254037844428154, -1.500000000000001332 ) ) ;
#1295=CARTESIAN_POINT ( 'NONE',  ( 1.560000000000005826, 0.000000000000000000, 0.000000000000000000 ) ) ;
#1305=ORIENTED_EDGE ( 'NONE', *, *, #11754, .F. ) ;
#1310=EDGE_CURVE ( 'NONE', #6345, #11793, #5286, .T. ) ;
#1326=VERTEX_POINT ( 'NONE', #2147 ) ;
#1336=AXIS2_PLACEMENT_3D ( 'NONE', #10596, #6410, #11911 ) ;
#1337=CARTESIAN_POINT ( 'NONE',  ( 2.369999999999996998, 5.817072295949927426E-16, -4.750000000000000000 ) ) ;
#1341=VERTEX_POINT ( 'NONE', #11070 ) ;
#1346=DIRECTION ( 'NONE',  ( 0.000000000000000000, 0.000000000000000000, 1.000000000000000000 ) ) ;
#1353=CARTESIAN_POINT ( 'NONE',  ( 1.560000000000005826, 0.000000000000000000, -1.500000000000001332 ) ) ;
#1398=AXIS2_PLACEMENT_3D ( 'NONE', #8081, #3866, #8300 ) ;
#1423=LINE ( 'NONE', #1283, #5753 ) ;
#1450=CIRCLE ( 'NONE', #10572, 1.500000000000000000 ) ;
#1467=PRODUCT_DEFINITION_SHAPE ( 'NONE', 'NONE',  #13858 ) ;
#1472=ORIENTED_EDGE ( 'NONE', *, *, #10760, .F. ) ;
#1473=AXIS2_PLACEMENT_3D ( 'NONE', #14275, #4336, #8771 ) ;
#1482=CIRCLE ( 'NONE', #2415, 2.499999999999999556 ) ;
#1489=DIRECTION ( 'NONE',  ( -1.000000000000000000, 0.000000000000000000, 0.000000000000000000 ) ) ;
#1495=CARTESIAN_POINT ( 'NONE',  ( 2.369999999999996998, 0.000000000000000000, 0.000000000000000000 ) ) ;
#1544=FILL_AREA_STYLE ('',( #13860 ) ) ;
#1610=ORIENTED_EDGE ( 'NONE', *, *, #2488, .T. ) ;
#1611=EDGE_CURVE ( 'NONE', #1181, #588, #7961, .T. ) ;
#1614=PLANE ( 'NONE',  #3089 ) ;
#1621=CARTESIAN_POINT ( 'NONE',  ( 0.000000000000000000, 3.061616997868382155E-16, -2.499999999999999112 ) ) ;
#1653=AXIS2_PLACEMENT_3D ( 'NONE', #964, #8726, #8862 ) ;
#1677=MECHANICAL_DESIGN_GEOMETRIC_PRESENTATION_REPRESENTATION('',(#4032),#3781);
#1690=CIRCLE ( 'NONE', #2874, 4.750000000000000000 ) ;
#1728=ORIENTED_EDGE ( 'NONE', *, *, #13993, .T. ) ;
#1765=ADVANCED_FACE ( 'NONE', ( #2727, #3030 ), #1614, .T. ) ;
#1794=DIRECTION ( 'NONE',  ( 0.000000000000000000, 0.000000000000000000, 1.000000000000000000 ) ) ;
#1799=ORIENTED_EDGE ( 'NONE', *, *, #9028, .F. ) ;
#1810=DIRECTION ( 'NONE',  ( 0.000000000000000000, 0.000000000000000000, 1.000000000000000000 ) ) ;
#1822=ORIENTED_EDGE ( 'NONE', *, *, #6939, .F. ) ;
#1841=ORIENTED_EDGE ( 'NONE', *, *, #1611, .T. ) ;
#1861=VERTEX_POINT ( 'NONE', #4274 ) ;
#1872=CYLINDRICAL_SURFACE ( 'NONE', #9645, 4.750000000000000000 ) ;
#1890=AXIS2_PLACEMENT_3D ( 'NONE', #7851, #2239, #984 ) ;
#1899=VECTOR ( 'NONE', #1028, 1000.000000000000114 ) ;
#1961=CARTESIAN_POINT ( 'NONE',  ( 1.560000000000005826, -0.8660254037844428154, -1.500000000000001332 ) ) ;
#1988=DIRECTION ( 'NONE',  ( -1.000000000000000000, 0.000000000000000000, 0.000000000000000000 ) ) ;
#2012=ORIENTED_EDGE ( 'NONE', *, *, #12789, .F. ) ;
#2017=ORIENTED_EDGE ( 'NONE', *, *, #11143, .T. ) ;
#2060=VECTOR ( 'NONE', #6406, 1000.000000000000114 ) ;
#2075=CIRCLE ( 'NONE', #10242, 2.055000000000000160 ) ;
#2147=CARTESIAN_POINT ( 'NONE',  ( 1.560000000000005826, 0.8660254037844428154, -1.500000000000001332 ) ) ;
#2153=COLOUR_RGB ( '', 0.66274510, 0.83137255, 0.94901961) ;
#2154=VECTOR ( 'NONE', #12374, 1000.000000000000000 ) ;
#2165=ORIENTED_EDGE ( 'NONE', *, *, #4591, .F. ) ;
#2175=AXIS2_PLACEMENT_3D ( 'NONE', #7594, #1988, #6429 ) ;
#2180=CARTESIAN_POINT ( 'NONE',  ( 2.369999999999996998, 0.000000000000000000, 0.000000000000000000 ) ) ;
#2183=ORIENTED_EDGE ( 'NONE', *, *, #13023, .T. ) ;
#2239=DIRECTION ( 'NONE',  ( -1.000000000000000000, 0.000000000000000000, 0.000000000000000000 ) ) ;
#2250=VECTOR ( 'NONE', #18, 1000.000000000000000 ) ;
#2252=ORIENTED_EDGE ( 'NONE', *, *, #3650, .F. ) ;
#2273=DIRECTION ( 'NONE',  ( 0.000000000000000000, -1.000000000000000000, 0.000000000000000000 ) ) ;
#2291=AXIS2_PLACEMENT_3D ( 'NONE', #13312, #5264, #4182 ) ;
#2322=VECTOR ( 'NONE', #4576, 1000.000000000000000 ) ;
#2336=ORIENTED_EDGE ( 'NONE', *, *, #3180, .T. ) ;
#2351=DIRECTION ( 'NONE',  ( 0.000000000000000000, 0.000000000000000000, 1.000000000000000000 ) ) ;
#2386=AXIS2_PLACEMENT_3D ( 'NONE', #9727, #11705, #9515 ) ;
#2387=CARTESIAN_POINT ( 'NONE',  ( 1.560000000000005826, -1.732050807568885631, 0.000000000000000000 ) ) ;
#2388=EDGE_LOOP ( 'NONE', ( #8972, #10139, #12616, #7615, #6326 ) ) ;
#2415=AXIS2_PLACEMENT_3D ( 'NONE', #14438, #12160, #9966 ) ;
#2419=DIRECTION ( 'NONE',  ( 0.000000000000000000, 0.000000000000000000, 1.000000000000000000 ) ) ;
#2437=ADVANCED_FACE ( 'NONE', ( #4468 ), #168, .F. ) ;
#2456=CARTESIAN_POINT ( 'NONE',  ( 2.949999999999994404, 0.000000000000000000, 0.000000000000000000 ) ) ;
#2465=CARTESIAN_POINT ( 'NONE',  ( 1.560000000000005826, -1.732050807568885631, 0.000000000000000000 ) ) ;
#2468=CARTESIAN_POINT ( 'NONE',  ( 2.369999999999996998, 0.000000000000000000, 0.000000000000000000 ) ) ;
#2488=EDGE_CURVE ( 'NONE', #12697, #2567, #2075, .T. ) ;
#2524=DIRECTION ( 'NONE',  ( -1.000000000000000000, 0.000000000000000000, 0.000000000000000000 ) ) ;
#2564=CIRCLE ( 'NONE', #3503, 2.699999999999999289 ) ;
#2567=VERTEX_POINT ( 'NONE', #10432 ) ;
#2605=ORIENTED_EDGE ( 'NONE', *, *, #12783, .T. ) ;
#2607=DIRECTION ( 'NONE',  ( -1.000000000000000000, 0.000000000000000000, 0.000000000000000000 ) ) ;
#2661=ORIENTED_EDGE ( 'NONE', *, *, #12092, .F. ) ;
#2662=ADVANCED_FACE ( 'NONE', ( #14250 ), #9709, .T. ) ;
#2665=UNCERTAINTY_MEASURE_WITH_UNIT (LENGTH_MEASURE( 1.000000000000000082E-05 ), #2975, 'distance_accuracy_value', 'NONE');
#2697=DIRECTION ( 'NONE',  ( 1.000000000000000000, 0.000000000000000000, 0.000000000000000000 ) ) ;
#2724=VERTEX_POINT ( 'NONE', #6899 ) ;
#2727=FACE_OUTER_BOUND ( 'NONE', #642, .T. ) ;
#2733=LINE ( 'NONE', #6069, #14313 ) ;
#2740=DIRECTION ( 'NONE',  ( 0.000000000000000000, -0.000000000000000000, 1.000000000000000000 ) ) ;
#2749=SURFACE_STYLE_FILL_AREA ( #6088 ) ;
#2800=FACE_OUTER_BOUND ( 'NONE', #8243, .T. ) ;
#2810=ORIENTED_EDGE ( 'NONE', *, *, #7459, .F. ) ;
#2850=CARTESIAN_POINT ( 'NONE',  ( 4.755015822784813828, 0.000000000000000000, 0.000000000000000000 ) ) ;
#2874=AXIS2_PLACEMENT_3D ( 'NONE', #1495, #4856, #1794 ) ;
#2883=AXIS2_PLACEMENT_3D ( 'NONE', #11718, #12079, #8988 ) ;
#2892=VECTOR ( 'NONE', #6643, 1000.000000000000114 ) ;
#2895=CARTESIAN_POINT ( 'NONE',  ( 1.560000000000005826, -0.8660254037844428154, -1.500000000000001332 ) ) ;
#2918=VERTEX_POINT ( 'NONE', #6008 ) ;
#2919=CARTESIAN_POINT ( 'NONE',  ( 2.949999999999994404, 0.000000000000000000, 0.000000000000000000 ) ) ;
#2936=DIRECTION ( 'NONE',  ( -1.000000000000000000, 0.000000000000000000, 0.000000000000000000 ) ) ;
#2970=EDGE_LOOP ( 'NONE', ( #8126, #1472, #6691 ) ) ;
#2975=( LENGTH_UNIT ( ) NAMED_UNIT ( * ) SI_UNIT ( .MILLI., .METRE. ) );
#3016=DIRECTION ( 'NONE',  ( -1.000000000000000000, 0.000000000000000000, 0.000000000000000000 ) ) ;
#3023=ORIENTED_EDGE ( 'NONE', *, *, #10591, .F. ) ;
#3026=AXIS2_PLACEMENT_3D ( 'NONE', #9923, #3139, #9633 ) ;
#3030=FACE_BOUND ( 'NONE', #12290, .T. ) ;
#3069=CARTESIAN_POINT ( 'NONE',  ( 2.369999999999996998, 4.749999999999999112, 0.000000000000000000 ) ) ;
#3089=AXIS2_PLACEMENT_3D ( 'NONE', #8497, #10767, #11719 ) ;
#3105=LINE ( 'NONE', #13262, #13062 ) ;
#3108=DIRECTION ( 'NONE',  ( -1.000000000000000000, 0.000000000000000000, 0.000000000000000000 ) ) ;
#3119=ORIENTED_EDGE ( 'NONE', *, *, #12620, .F. ) ;
#3137=CONICAL_SURFACE ( 'NONE', #14122, 2.055000000000000160, 0.7853981633974428389 ) ;
#3139=DIRECTION ( 'NONE',  ( 0.000000000000000000, -0.8660254037844388186, -0.4999999999999998335 ) ) ;
#3175=CARTESIAN_POINT ( 'NONE',  ( 1.560000000000005826, 1.732050807568871864, 0.000000000000000000 ) ) ;
#3180=EDGE_CURVE ( 'NONE', #3412, #1341, #11596, .T. ) ;
#3202=ORIENTED_EDGE ( 'NONE', *, *, #14383, .T. ) ;
#3233=DIRECTION ( 'NONE',  ( 0.000000000000000000, 1.000000000000000000, 1.224646799147353207E-16 ) ) ;
#3285=VERTEX_POINT ( 'NONE', #10039 ) ;
#3286=CARTESIAN_POINT ( 'NONE',  ( 27.75000000000001066, 0.000000000000000000, 0.000000000000000000 ) ) ;
#3295=AXIS2_PLACEMENT_3D ( 'NONE', #10853, #2740, #14161 ) ;
#3309=VECTOR ( 'NONE', #12595, 1000.000000000000000 ) ;
#3330=VECTOR ( 'NONE', #3682, 1000.000000000000000 ) ;
#3383=CARTESIAN_POINT ( 'NONE',  ( 0.000000000000000000, 0.8660254037844428154, 1.500000000000001332 ) ) ;
#3412=VERTEX_POINT ( 'NONE', #11452 ) ;
#3447=DIRECTION ( 'NONE',  ( 0.000000000000000000, -0.4999999999999997224, 0.8660254037844387076 ) ) ;
#3455=LINE ( 'NONE', #7900, #2154 ) ;
#3462=VECTOR ( 'NONE', #8588, 1000.000000000000114 ) ;
#3483=CARTESIAN_POINT ( 'NONE',  ( 0.000000000000000000, 0.000000000000000000, 4.750000000000000000 ) ) ;
#3491=DIRECTION ( 'NONE',  ( -1.000000000000000000, 0.000000000000000000, 0.000000000000000000 ) ) ;
#3503=AXIS2_PLACEMENT_3D ( 'NONE', #4036, #7376, #10827 ) ;
#3504=DIRECTION ( 'NONE',  ( -1.000000000000000000, 0.000000000000000000, 0.000000000000000000 ) ) ;
#3529=CARTESIAN_POINT ( 'NONE',  ( 0.000000000000000000, -0.8660254037844428154, 1.500000000000001332 ) ) ;
#3531=VECTOR ( 'NONE', #2273, 1000.000000000000000 ) ;
#3544=TOROIDAL_SURFACE ( 'NONE', #4005, 2.699999999999999289, 0.2000000000000000111 ) ;
#3576=FACE_OUTER_BOUND ( 'NONE', #12792, .T. ) ;
#3590=ORIENTED_EDGE ( 'NONE', *, *, #13601, .T. ) ;
#3605=ORIENTED_EDGE ( 'NONE', *, *, #3650, .T. ) ;
#3650=EDGE_CURVE ( 'NONE', #4944, #11701, #5582, .T. ) ;
#3682=DIRECTION ( 'NONE',  ( -1.000000000000000000, 0.000000000000000000, 0.000000000000000000 ) ) ;
#3705=DIRECTION ( 'NONE',  ( -1.000000000000000000, 0.000000000000000000, 0.000000000000000000 ) ) ;
#3748=DIRECTION ( 'NONE',  ( -1.000000000000000000, 0.000000000000000000, 0.000000000000000000 ) ) ;
#3749=PRESENTATION_STYLE_ASSIGNMENT (( #611 ) ) ;
#3758=ORIENTED_EDGE ( 'NONE', *, *, #9882, .F. ) ;
#3774=CARTESIAN_POINT ( 'NONE',  ( 27.75000000000001066, 0.000000000000000000, 0.000000000000000000 ) ) ;
#3781=( GEOMETRIC_REPRESENTATION_CONTEXT ( 3 ) GLOBAL_UNCERTAINTY_ASSIGNED_CONTEXT ( ( #8647 ) ) GLOBAL_UNIT_ASSIGNED_CONTEXT ( ( #6065, #455, #534 ) ) REPRESENTATION_CONTEXT ( 'NONE', 'WORKASPACE' ) );
#3854=FILL_AREA_STYLE_COLOUR ( '', #24 ) ;
#3865=SHAPE_REPRESENTATION ( 'socket button head screw_iso_ISO 7380 - M5 x 25 - 25N', ( #11025 ), #10079 ) ;
#3866=DIRECTION ( 'NONE',  ( 0.000000000000000000, 0.000000000000000000, 1.000000000000000000 ) ) ;
#3925=EDGE_LOOP ( 'NONE', ( #11519, #5194, #110, #856, #383 ) ) ;
#3930=AXIS2_PLACEMENT_3D ( 'NONE', #2468, #13531, #12423 ) ;
#4001=FACE_OUTER_BOUND ( 'NONE', #12740, .T. ) ;
#4005=AXIS2_PLACEMENT_3D ( 'NONE', #8064, #8215, #1209 ) ;
#4009=ADVANCED_FACE ( 'NONE', ( #5218 ), #12030, .T. ) ;
#4012=CARTESIAN_POINT ( 'NONE',  ( 27.75000000000001066, 0.000000000000000000, 0.000000000000000000 ) ) ;
#4032=STYLED_ITEM ( 'NONE', ( #3749 ), #10469 ) ;
#4036=CARTESIAN_POINT ( 'NONE',  ( 2.750000000000002665, 0.000000000000000000, 0.000000000000000000 ) ) ;
#4046=AXIS2_PLACEMENT_3D ( 'NONE', #10169, #1099, #9958 ) ;
#4050=ORIENTED_EDGE ( 'NONE', *, *, #1611, .F. ) ;
#4063=ORIENTED_EDGE ( 'NONE', *, *, #6939, .T. ) ;
#4098=VERTEX_POINT ( 'NONE', #5432 ) ;
#4099=CARTESIAN_POINT ( 'NONE',  ( 1.560000000000005826, 0.8660254037844428154, 1.500000000000001332 ) ) ;
#4108=EDGE_CURVE ( 'NONE', #1341, #2724, #14441, .T. ) ;
#4147=VERTEX_POINT ( 'NONE', #7910 ) ;
#4148=SURFACE_STYLE_USAGE ( .BOTH. , #11585 ) ;
#4167=ORIENTED_EDGE ( 'NONE', *, *, #7818, .T. ) ;
#4182=DIRECTION ( 'NONE',  ( 0.000000000000000000, 0.000000000000000000, 1.000000000000000000 ) ) ;
#4195=ORIENTED_EDGE ( 'NONE', *, *, #13347, .T. ) ;
#4274=CARTESIAN_POINT ( 'NONE',  ( 0.000000000000000000, -1.732050807568885631, 0.000000000000000000 ) ) ;
#4318=CARTESIAN_POINT ( 'NONE',  ( 0.000000000000000000, 0.000000000000000000, 0.000000000000000000 ) ) ;
#4335=EDGE_LOOP ( 'NONE', ( #6126, #1610, #13908, #11375 ) ) ;
#4336=DIRECTION ( 'NONE',  ( 0.000000000000000000, 0.8660254037844380415, 0.5000000000000011102 ) ) ;
#4372=EDGE_LOOP ( 'NONE', ( #7484, #11615, #2605, #5588 ) ) ;
#4415=CARTESIAN_POINT ( 'NONE',  ( 0.000000000000000000, 0.000000000000000000, 0.000000000000000000 ) ) ;
#4421=AXIS2_PLACEMENT_3D ( 'NONE', #11579, #12599, #10488 ) ;
#4428=CARTESIAN_POINT ( 'NONE',  ( 27.75000000000001066, 2.516649172247811061E-16, -2.055000000000000160 ) ) ;
#4433=ADVANCED_FACE ( 'NONE', ( #2800 ), #7240, .F. ) ;
#4468=FACE_OUTER_BOUND ( 'NONE', #306, .T. ) ;
#4492=DIRECTION ( 'NONE',  ( -1.000000000000000000, 0.000000000000000000, 0.000000000000000000 ) ) ;
#4505=FACE_OUTER_BOUND ( 'NONE', #12633, .T. ) ;
#4539=DIRECTION ( 'NONE',  ( 0.000000000000000000, -1.000000000000000000, 0.000000000000000000 ) ) ;
#4550=AXIS2_PLACEMENT_3D ( 'NONE', #2919, #7356, #11831 ) ;
#4564=CIRCLE ( 'NONE', #4550, 2.499999999999999112 ) ;
#4576=DIRECTION ( 'NONE',  ( -0.7071067811865513475, 0.000000000000000000, 0.7071067811865436870 ) ) ;
#4579=APPLICATION_CONTEXT ( 'automotive_design' ) ;
#4591=EDGE_CURVE ( 'NONE', #11701, #8874, #11748, .T. ) ;
#4594=DIRECTION ( 'NONE',  ( 0.000000000000000000, 0.000000000000000000, 1.000000000000000000 ) ) ;
#4629=EDGE_LOOP ( 'NONE', ( #4869, #1192 ) ) ;
#4653=ORIENTED_EDGE ( 'NONE', *, *, #11313, .F. ) ;
#4658=ORIENTED_EDGE ( 'NONE', *, *, #8473, .F. ) ;
#4698=ORIENTED_EDGE ( 'NONE', *, *, #8453, .T. ) ;
#4709=LINE ( 'NONE', #1621, #3330 ) ;
#4751=CARTESIAN_POINT ( 'NONE',  ( 2.426025403784448642, 2.655529440325959183E-32, -2.168404344971008868E-16 ) ) ;
#4757=CIRCLE ( 'NONE', #8495, 2.055000000000000160 ) ;
#4780=DIRECTION ( 'NONE',  ( 0.000000000000000000, -0.4999999999999997224, 0.8660254037844387076 ) ) ;
#4856=DIRECTION ( 'NONE',  ( -1.000000000000000000, 0.000000000000000000, 0.000000000000000000 ) ) ;
#4869=ORIENTED_EDGE ( 'NONE', *, *, #14344, .F. ) ;
#4925=CIRCLE ( 'NONE', #14290, 5.315148208181398104 ) ;
#4935=DIRECTION ( 'NONE',  ( 0.000000000000000000, 0.000000000000000000, 1.000000000000000000 ) ) ;
#4944=VERTEX_POINT ( 'NONE', #5785 ) ;
#4948=ORIENTED_EDGE ( 'NONE', *, *, #773, .F. ) ;
#4992=( LENGTH_UNIT ( ) NAMED_UNIT ( * ) SI_UNIT ( .MILLI., .METRE. ) );
#5001=AXIS2_PLACEMENT_3D ( 'NONE', #569, #2607, #10658 ) ;
#5050=CARTESIAN_POINT ( 'NONE',  ( 2.949999999999994404, 0.000000000000000000, 2.499999999999999112 ) ) ;
#5058=CARTESIAN_POINT ( 'NONE',  ( 0.000000000000000000, 1.732050807568871864, 0.000000000000000000 ) ) ;
#5100=EDGE_CURVE ( 'NONE', #13268, #4944, #11818, .T. ) ;
#5116=ADVANCED_FACE ( 'NONE', ( #9390 ), #324, .F. ) ;
#5137=LINE ( 'NONE', #3175, #10119 ) ;
#5141=UNCERTAINTY_MEASURE_WITH_UNIT (LENGTH_MEASURE( 1.000000000000000082E-05 ), #4992, 'distance_accuracy_value', 'NONE');
#5166=CARTESIAN_POINT ( 'NONE',  ( 0.000000000000000000, -1.732050807568885631, 0.000000000000000000 ) ) ;
#5185=CIRCLE ( 'NONE', #4046, 0.2000000000000000944 ) ;
#5194=ORIENTED_EDGE ( 'NONE', *, *, #9461, .T. ) ;
#5198=ORIENTED_EDGE ( 'NONE', *, *, #9882, .T. ) ;
#5215=VERTEX_POINT ( 'NONE', #14020 ) ;
#5218=FACE_OUTER_BOUND ( 'NONE', #2388, .T. ) ;
#5228=ORIENTED_EDGE ( 'NONE', *, *, #12022, .F. ) ;
#5233=ORIENTED_EDGE ( 'NONE', *, *, #11313, .T. ) ;
#5235=DIRECTION ( 'NONE',  ( 0.000000000000000000, 0.000000000000000000, 1.000000000000000000 ) ) ;
#5249=VERTEX_POINT ( 'NONE', #11814 ) ;
#5264=DIRECTION ( 'NONE',  ( -1.000000000000000000, 0.000000000000000000, 0.000000000000000000 ) ) ;
#5265=SPHERICAL_SURFACE ( 'NONE', #962, 5.315148208181398104 ) ;
#5281=DIRECTION ( 'NONE',  ( -1.000000000000000000, 0.000000000000000000, 0.000000000000000000 ) ) ;
#5286=LINE ( 'NONE', #2895, #12404 ) ;
#5287=DIRECTION ( 'NONE',  ( 0.000000000000000000, -0.8660254037844388186, 0.4999999999999996114 ) ) ;
#5327=CARTESIAN_POINT ( 'NONE',  ( 1.560000000000005826, -0.8660254037844428154, -1.500000000000001332 ) ) ;
#5386=CIRCLE ( 'NONE', #21, 0.2000000000000000944 ) ;
#5402=( GEOMETRIC_REPRESENTATION_CONTEXT ( 3 ) GLOBAL_UNCERTAINTY_ASSIGNED_CONTEXT ( ( #2665 ) ) GLOBAL_UNIT_ASSIGNED_CONTEXT ( ( #2975, #6174, #10648 ) ) REPRESENTATION_CONTEXT ( 'NONE', 'WORKASPACE' ) );
#5420=VECTOR ( 'NONE', #10553, 1000.000000000000114 ) ;
#5423=LINE ( 'NONE', #1106, #9398 ) ;
#5428=AXIS2_PLACEMENT_3D ( 'NONE', #12377, #12, #2351 ) ;
#5432=CARTESIAN_POINT ( 'NONE',  ( 1.560000000000005826, 1.299038105676664223, 0.7500000000000006661 ) ) ;
#5441=DIRECTION ( 'NONE',  ( 1.000000000000000000, 0.000000000000000000, 0.000000000000000000 ) ) ;
#5483=VERTEX_POINT ( 'NONE', #8620 ) ;
#5486=CARTESIAN_POINT ( 'NONE',  ( 0.000000000000000000, -0.8660254037844428154, -1.500000000000001332 ) ) ;
#5509=DIRECTION ( 'NONE',  ( -1.000000000000000000, 0.000000000000000000, 0.000000000000000000 ) ) ;
#5562=DIRECTION ( 'NONE',  ( -0.000000000000000000, -0.5000000000000011102, -0.8660254037844379305 ) ) ;
#5582=LINE ( 'NONE', #3483, #1211 ) ;
#5588=ORIENTED_EDGE ( 'NONE', *, *, #773, .T. ) ;
#5592=ADVANCED_FACE ( 'NONE', ( #7728 ), #5598, .T. ) ;
#5598=CONICAL_SURFACE ( 'NONE', #227, 2.055000000000000160, 0.7853981633974428389 ) ;
#5612=CARTESIAN_POINT ( 'NONE',  ( 2.426025403784448642, 0.000000000000000000, 2.168404344971008868E-16 ) ) ;
#5620=VECTOR ( 'NONE', #3491, 1000.000000000000000 ) ;
#5650=EDGE_CURVE ( 'NONE', #4147, #13213, #12277, .T. ) ;
#5657=CIRCLE ( 'NONE', #6370, 2.375000000000000000 ) ;
#5658=EDGE_LOOP ( 'NONE', ( #4698, #586, #3202, #13100, #11887 ) ) ;
#5661=EDGE_LOOP ( 'NONE', ( #10429, #2183, #5228, #11184 ) ) ;
#5678=PRODUCT_DEFINITION_FORMATION_WITH_SPECIFIED_SOURCE ( 'ANY', '', #13505, .NOT_KNOWN. ) ;
#5708=ADVANCED_FACE ( 'NONE', ( #12703 ), #9412, .T. ) ;
#5711=ORIENTED_EDGE ( 'NONE', *, *, #8453, .F. ) ;
#5719=CARTESIAN_POINT ( 'NONE',  ( 1.560000000000005826, 1.732050807568871864, 0.000000000000000000 ) ) ;
#5727=ORIENTED_EDGE ( 'NONE', *, *, #12789, .T. ) ;
#5738=DIRECTION ( 'NONE',  ( -1.000000000000000000, 0.000000000000000000, 0.000000000000000000 ) ) ;
#5744=ORIENTED_EDGE ( 'NONE', *, *, #5650, .T. ) ;
#5753=VECTOR ( 'NONE', #11590, 1000.000000000000000 ) ;
#5785=CARTESIAN_POINT ( 'NONE',  ( 2.750000000000002665, 0.000000000000000000, 4.750000000000000000 ) ) ;
#5805=ADVANCED_FACE ( 'NONE', ( #3576 ), #7130, .T. ) ;
#5834=PRODUCT_DEFINITION_CONTEXT ( 'detailed design', #10632, 'design' ) ;
#5836=ORIENTED_EDGE ( 'NONE', *, *, #5890, .T. ) ;
#5838=CARTESIAN_POINT ( 'NONE',  ( 1.560000000000005826, 0.000000000000000000, 0.000000000000000000 ) ) ;
#5853=AXIS2_PLACEMENT_3D ( 'NONE', #598, #3016, #8554 ) ;
#5868=CARTESIAN_POINT ( 'NONE',  ( 0.000000000000000000, 0.000000000000000000, 0.000000000000000000 ) ) ;
#5885=DIRECTION ( 'NONE',  ( 0.000000000000000000, 0.000000000000000000, 1.000000000000000000 ) ) ;
#5890=EDGE_CURVE ( 'NONE', #8562, #4098, #647, .T. ) ;
#5921=SURFACE_STYLE_FILL_AREA ( #1544 ) ;
#5923=EDGE_CURVE ( 'NONE', #4098, #1181, #934, .T. ) ;
#5974=CARTESIAN_POINT ( 'NONE',  ( 27.75000000000001066, 0.000000000000000000, 2.055000000000000160 ) ) ;
#5994=CIRCLE ( 'NONE', #8102, 2.499999999999999112 ) ;
#5995=DIRECTION ( 'NONE',  ( -1.000000000000000000, 0.000000000000000000, 0.000000000000000000 ) ) ;
#6000=ADVANCED_FACE ( 'NONE', ( #6834 ), #11301, .F. ) ;
#6007=DIRECTION ( 'NONE',  ( 0.000000000000000000, 0.000000000000000000, 1.000000000000000000 ) ) ;
#6008=CARTESIAN_POINT ( 'NONE',  ( 2.369999999999996998, -4.749999999999999112, -5.817072295949926440E-16 ) ) ;
#6010=ORIENTED_EDGE ( 'NONE', *, *, #13601, .F. ) ;
#6018=DIRECTION ( 'NONE',  ( 0.000000000000000000, 0.000000000000000000, 1.000000000000000000 ) ) ;
#6029=DIRECTION ( 'NONE',  ( 0.000000000000000000, 0.5000000000000012212, 0.8660254037844380415 ) ) ;
#6065=( LENGTH_UNIT ( ) NAMED_UNIT ( * ) SI_UNIT ( .MILLI., .METRE. ) );
#6069=CARTESIAN_POINT ( 'NONE',  ( 0.000000000000000000, 0.000000000000000000, 2.499999999999999112 ) ) ;
#6071=LINE ( 'NONE', #389, #10360 ) ;
#6083=ORIENTED_EDGE ( 'NONE', *, *, #10672, .T. ) ;
#6088=FILL_AREA_STYLE ('',( #3854 ) ) ;
#6092=DIRECTION ( 'NONE',  ( -1.000000000000000000, 0.000000000000000000, 0.000000000000000000 ) ) ;
#6118=VERTEX_POINT ( 'NONE', #1337 ) ;
#6122=VECTOR ( 'NONE', #14437, 1000.000000000000000 ) ;
#6126=ORIENTED_EDGE ( 'NONE', *, *, #13023, .F. ) ;
#6140=EDGE_CURVE ( 'NONE', #8874, #10551, #11225, .T. ) ;
#6165=DIRECTION ( 'NONE',  ( -1.000000000000000000, 0.000000000000000000, 0.000000000000000000 ) ) ;
#6174=( NAMED_UNIT ( * ) PLANE_ANGLE_UNIT ( ) SI_UNIT ( $, .RADIAN. ) );
#6219=ORIENTED_EDGE ( 'NONE', *, *, #9461, .F. ) ;
#6234=CARTESIAN_POINT ( 'NONE',  ( 1.560000000000005826, 1.732050807568871864, 0.000000000000000000 ) ) ;
#6239=VERTEX_POINT ( 'NONE', #7690 ) ;
#6272=ORIENTED_EDGE ( 'NONE', *, *, #8315, .F. ) ;
#6289=ADVANCED_FACE ( 'NONE', ( #4505 ), #14281, .F. ) ;
#6301=CARTESIAN_POINT ( 'NONE',  ( 27.75000000000001066, 0.000000000000000000, 0.000000000000000000 ) ) ;
#6326=ORIENTED_EDGE ( 'NONE', *, *, #14383, .F. ) ;
#6345=VERTEX_POINT ( 'NONE', #10916 ) ;
#6368=EDGE_CURVE ( 'NONE', #2567, #5483, #514, .T. ) ;
#6370=AXIS2_PLACEMENT_3D ( 'NONE', #1233, #3705, #6018 ) ;
#6390=ORIENTED_EDGE ( 'NONE', *, *, #10673, .T. ) ;
#6406=DIRECTION ( 'NONE',  ( 0.000000000000000000, 0.5000000000000011102, -0.8660254037844379305 ) ) ;
#6410=DIRECTION ( 'NONE',  ( 1.000000000000000000, 0.000000000000000000, 0.000000000000000000 ) ) ;
#6420=FACE_OUTER_BOUND ( 'NONE', #189, .T. ) ;
#6429=DIRECTION ( 'NONE',  ( 0.000000000000000000, 0.000000000000000000, 1.000000000000000000 ) ) ;
#6524=DIRECTION ( 'NONE',  ( 0.000000000000000000, 0.000000000000000000, 1.000000000000000000 ) ) ;
#6593=DIRECTION ( 'NONE',  ( -1.000000000000000000, 0.000000000000000000, 0.000000000000000000 ) ) ;
#6619=VECTOR ( 'NONE', #11261, 1000.000000000000114 ) ;
#6620=EDGE_CURVE ( 'NONE', #13071, #6239, #2564, .T. ) ;
#6629=ORIENTED_EDGE ( 'NONE', *, *, #125, .T. ) ;
#6643=DIRECTION ( 'NONE',  ( -0.5000000000000042188, 0.000000000000000000, 0.8660254037844361541 ) ) ;
#6691=ORIENTED_EDGE ( 'NONE', *, *, #13993, .F. ) ;
#6722=LINE ( 'NONE', #5486, #1899 ) ;
#6734=FACE_BOUND ( 'NONE', #14243, .T. ) ;
#6760=LINE ( 'NONE', #5719, #5620 ) ;
#6779=DIRECTION ( 'NONE',  ( 0.000000000000000000, 0.000000000000000000, -1.000000000000000000 ) ) ;
#6784=AXIS2_PLACEMENT_3D ( 'NONE', #6962, #7108, #10412 ) ;
#6834=FACE_OUTER_BOUND ( 'NONE', #837, .T. ) ;
#6843=ORIENTED_EDGE ( 'NONE', *, *, #9210, .F. ) ;
#6852=DIRECTION ( 'NONE',  ( -1.000000000000000000, 0.000000000000000000, 0.000000000000000000 ) ) ;
#6863=VECTOR ( 'NONE', #10934, 1000.000000000000114 ) ;
#6881=CARTESIAN_POINT ( 'NONE',  ( 2.750000000000002665, 5.817072295949927426E-16, -4.750000000000000000 ) ) ;
#6882=ORIENTED_EDGE ( 'NONE', *, *, #5100, .F. ) ;
#6899=CARTESIAN_POINT ( 'NONE',  ( 1.560000000000005826, -0.8660254037844428154, 1.500000000000001332 ) ) ;
#6906=ORIENTED_EDGE ( 'NONE', *, *, #10678, .T. ) ;
#6907=DIRECTION ( 'NONE',  ( 1.000000000000000000, -0.000000000000000000, -0.000000000000000000 ) ) ;
#6914=DIRECTION ( 'NONE',  ( 0.000000000000000000, 0.8660254037844380415, -0.5000000000000012212 ) ) ;
#6939=EDGE_CURVE ( 'NONE', #5249, #4147, #7820, .T. ) ;
#6960=CARTESIAN_POINT ( 'NONE',  ( 1.560000000000005826, -0.8660254037844428154, 1.500000000000001332 ) ) ;
#6962=CARTESIAN_POINT ( 'NONE',  ( 1.560000000000005826, -1.732050807568885631, 0.000000000000000000 ) ) ;
#7022=ORIENTED_EDGE ( 'NONE', *, *, #6620, .T. ) ;
#7108=DIRECTION ( 'NONE',  ( 1.000000000000000000, 0.000000000000000000, 0.000000000000000000 ) ) ;
#7116=ADVANCED_FACE ( 'NONE', ( #7573 ), #12055, .T. ) ;
#7130=PLANE ( 'NONE',  #9593 ) ;
#7168=LINE ( 'NONE', #10251, #5420 ) ;
#7240=PLANE ( 'NONE',  #2883 ) ;
#7275=CIRCLE ( 'NONE', #5853, 1.500000000000000000 ) ;
#7295=DIRECTION ( 'NONE',  ( 0.000000000000000000, 1.224646799147353207E-16, -1.000000000000000000 ) ) ;
#7319=DIRECTION ( 'NONE',  ( 0.000000000000000000, 0.000000000000000000, 1.000000000000000000 ) ) ;
#7356=DIRECTION ( 'NONE',  ( 1.000000000000000000, -0.000000000000000000, -0.000000000000000000 ) ) ;
#7376=DIRECTION ( 'NONE',  ( -1.000000000000000000, 0.000000000000000000, 0.000000000000000000 ) ) ;
#7397=DIRECTION ( 'NONE',  ( 0.000000000000000000, 0.4999999999999996669, 0.8660254037844388186 ) ) ;
#7404=ORIENTED_EDGE ( 'NONE', *, *, #824, .T. ) ;
#7414=CIRCLE ( 'NONE', #9294, 4.750000000000000000 ) ;
#7459=EDGE_CURVE ( 'NONE', #4944, #13268, #7414, .T. ) ;
#7466=CARTESIAN_POINT ( 'NONE',  ( 1.560000000000005826, 0.000000000000000000, 0.000000000000000000 ) ) ;
#7479=DIRECTION ( 'NONE',  ( -1.000000000000000000, 0.000000000000000000, 0.000000000000000000 ) ) ;
#7484=ORIENTED_EDGE ( 'NONE', *, *, #12835, .F. ) ;
#7497=AXIS2_PLACEMENT_3D ( 'NONE', #10238, #4492, #2419 ) ;
#7573=FACE_OUTER_BOUND ( 'NONE', #8865, .T. ) ;
#7590=ORIENTED_EDGE ( 'NONE', *, *, #7969, .T. ) ;
#7594=CARTESIAN_POINT ( 'NONE',  ( 2.369999999999996998, 0.000000000000000000, 0.000000000000000000 ) ) ;
#7596=LINE ( 'NONE', #1167, #3531 ) ;
#7615=ORIENTED_EDGE ( 'NONE', *, *, #7818, .F. ) ;
#7690=CARTESIAN_POINT ( 'NONE',  ( 2.749999999999998224, 3.306546357697852747E-16, -2.699999999999999289 ) ) ;
#7722=AXIS2_PLACEMENT_3D ( 'NONE', #579, #2697, #8305 ) ;
#7728=FACE_OUTER_BOUND ( 'NONE', #4335, .T. ) ;
#7741=ORIENTED_EDGE ( 'NONE', *, *, #14050, .F. ) ;
#7796=DIRECTION ( 'NONE',  ( 1.000000000000000000, 0.000000000000000000, 0.000000000000000000 ) ) ;
#7818=EDGE_CURVE ( 'NONE', #7871, #5249, #11725, .T. ) ;
#7820=LINE ( 'NONE', #3383, #13078 ) ;
#7851=CARTESIAN_POINT ( 'NONE',  ( 1.560000000000005826, 0.000000000000000000, 0.000000000000000000 ) ) ;
#7871=VERTEX_POINT ( 'NONE', #9891 ) ;
#7876=CARTESIAN_POINT ( 'NONE',  ( 1.560000000000005826, -1.732050807568885631, 0.000000000000000000 ) ) ;
#7900=CARTESIAN_POINT ( 'NONE',  ( 0.000000000000000000, 5.817072295949927426E-16, -4.750000000000000000 ) ) ;
#7906=FACE_OUTER_BOUND ( 'NONE', #9720, .T. ) ;
#7910=CARTESIAN_POINT ( 'NONE',  ( 0.000000000000000000, 0.8660254037844428154, 1.500000000000001332 ) ) ;
#7935=DIRECTION ( 'NONE',  ( -1.000000000000000000, 0.000000000000000000, 0.000000000000000000 ) ) ;
#7961=CIRCLE ( 'NONE', #10545, 1.500000000000000000 ) ;
#7969=EDGE_CURVE ( 'NONE', #14130, #1861, #3105, .T. ) ;
#7984=ORIENTED_EDGE ( 'NONE', *, *, #13048, .T. ) ;
#8036=EDGE_LOOP ( 'NONE', ( #11592, #8533, #9347, #4658 ) ) ;
#8064=CARTESIAN_POINT ( 'NONE',  ( 2.949999999999994404, 0.000000000000000000, 0.000000000000000000 ) ) ;
#8081=CARTESIAN_POINT ( 'NONE',  ( 1.560000000000005826, 0.8660254037844428154, -1.500000000000001332 ) ) ;
#8102=AXIS2_PLACEMENT_3D ( 'NONE', #2456, #6907, #11373 ) ;
#8119=ORIENTED_EDGE ( 'NONE', *, *, #10174, .F. ) ;
#8126=ORIENTED_EDGE ( 'NONE', *, *, #13347, .F. ) ;
#8196=SURFACE_SIDE_STYLE ('',( #5921 ) ) ;
#8215=DIRECTION ( 'NONE',  ( -1.000000000000000000, 0.000000000000000000, 0.000000000000000000 ) ) ;
#8243=EDGE_LOOP ( 'NONE', ( #4050, #56, #400 ) ) ;
#8287=PRESENTATION_STYLE_ASSIGNMENT (( #4148 ) ) ;
#8288=ORIENTED_EDGE ( 'NONE', *, *, #4108, .T. ) ;
#8300=DIRECTION ( 'NONE',  ( 1.000000000000000000, 0.000000000000000000, 0.000000000000000000 ) ) ;
#8305=DIRECTION ( 'NONE',  ( 0.000000000000000000, 0.000000000000000000, -1.000000000000000000 ) ) ;
#8309=ADVANCED_FACE ( 'NONE', ( #9856 ), #8819, .T. ) ;
#8315=EDGE_CURVE ( 'NONE', #6118, #2918, #12546, .T. ) ;
#8338=ADVANCED_FACE ( 'NONE', ( #14401 ), #8965, .F. ) ;
#8349=ORIENTED_EDGE ( 'NONE', *, *, #13491, .T. ) ;
#8418=ORIENTED_EDGE ( 'NONE', *, *, #7459, .T. ) ;
#8453=EDGE_CURVE ( 'NONE', #6345, #588, #1423, .T. ) ;
#8455=CARTESIAN_POINT ( 'NONE',  ( 0.000000000000000000, -2.375000000000000000, -4.362804221962446556E-16 ) ) ;
#8463=VECTOR ( 'NONE', #2524, 1000.000000000000000 ) ;
#8473=EDGE_CURVE ( 'NONE', #11431, #12337, #5994, .T. ) ;
#8495=AXIS2_PLACEMENT_3D ( 'NONE', #3774, #13730, #1346 ) ;
#8497=CARTESIAN_POINT ( 'NONE',  ( 0.000000000000000000, 0.000000000000000000, 0.000000000000000000 ) ) ;
#8533=ORIENTED_EDGE ( 'NONE', *, *, #6620, .F. ) ;
#8554=DIRECTION ( 'NONE',  ( 0.000000000000000000, 0.000000000000000000, 1.000000000000000000 ) ) ;
#8562=VERTEX_POINT ( 'NONE', #13076 ) ;
#8567=EDGE_CURVE ( 'NONE', #1326, #1181, #10863, .T. ) ;
#8588=DIRECTION ( 'NONE',  ( 0.000000000000000000, 0.4999999999999996669, 0.8660254037844388186 ) ) ;
#8592=AXIS2_PLACEMENT_3D ( 'NONE', #1295, #5738, #11390 ) ;
#8620=CARTESIAN_POINT ( 'NONE',  ( 27.30499999999998195, 0.000000000000000000, 2.499999999999999556 ) ) ;
#8636=ORIENTED_EDGE ( 'NONE', *, *, #9210, .T. ) ;
#8647=UNCERTAINTY_MEASURE_WITH_UNIT (LENGTH_MEASURE( 1.000000000000000082E-05 ), #6065, 'distance_accuracy_value', 'NONE');
#8695=DIRECTION ( 'NONE',  ( 0.000000000000000000, 0.5000000000000011102, -0.8660254037844379305 ) ) ;
#8726=DIRECTION ( 'NONE',  ( -1.000000000000000000, 0.000000000000000000, 0.000000000000000000 ) ) ;
#8754=CARTESIAN_POINT ( 'NONE',  ( 1.560000000000005826, -0.8660254037844428154, 1.500000000000001332 ) ) ;
#8771=DIRECTION ( 'NONE',  ( 0.000000000000000000, -0.5000000000000011102, 0.8660254037844380415 ) ) ;
#8787=CARTESIAN_POINT ( 'NONE',  ( 2.749999999999998224, 0.000000000000000000, 2.699999999999999289 ) ) ;
#8811=EDGE_CURVE ( 'NONE', #588, #375, #14447, .T. ) ;
#8819=PLANE ( 'NONE',  #12818 ) ;
#8825=ADVANCED_FACE ( 'NONE', ( #281 ), #353, .F. ) ;
#8862=DIRECTION ( 'NONE',  ( 0.000000000000000000, 0.000000000000000000, 1.000000000000000000 ) ) ;
#8865=EDGE_LOOP ( 'NONE', ( #8418, #9962, #6843, #2165, #2252 ) ) ;
#8874=VERTEX_POINT ( 'NONE', #3069 ) ;
#8894=VECTOR ( 'NONE', #1489, 1000.000000000000000 ) ;
#8965=PLANE ( 'NONE',  #10452 ) ;
#8972=ORIENTED_EDGE ( 'NONE', *, *, #8567, .T. ) ;
#8984=LINE ( 'NONE', #4751, #6619 ) ;
#8988=DIRECTION ( 'NONE',  ( 0.000000000000000000, 0.000000000000000000, -1.000000000000000000 ) ) ;
#9003=ADVANCED_FACE ( 'NONE', ( #6420 ), #12068, .T. ) ;
#9028=EDGE_CURVE ( 'NONE', #14130, #375, #9938, .T. ) ;
#9090=ORIENTED_EDGE ( 'NONE', *, *, #6140, .F. ) ;
#9132=LINE ( 'NONE', #13844, #14300 ) ;
#9138=AXIS2_PLACEMENT_3D ( 'NONE', #7876, #930, #6779 ) ;
#9150=CIRCLE ( 'NONE', #2386, 2.699999999999999289 ) ;
#9210=EDGE_CURVE ( 'NONE', #8874, #6118, #13983, .T. ) ;
#9294=AXIS2_PLACEMENT_3D ( 'NONE', #13360, #5509, #10859 ) ;
#9300=AXIS2_PLACEMENT_3D ( 'NONE', #12837, #10413, #6007 ) ;
#9347=ORIENTED_EDGE ( 'NONE', *, *, #12620, .T. ) ;
#9390=FACE_OUTER_BOUND ( 'NONE', #4629, .T. ) ;
#9398=VECTOR ( 'NONE', #5562, 1000.000000000000114 ) ;
#9412=PLANE ( 'NONE',  #1398 ) ;
#9452=( NAMED_UNIT ( * ) SI_UNIT ( $, .STERADIAN. ) SOLID_ANGLE_UNIT ( ) );
#9461=EDGE_CURVE ( 'NONE', #375, #6345, #11984, .T. ) ;
#9515=DIRECTION ( 'NONE',  ( 0.000000000000000000, 0.000000000000000000, 1.000000000000000000 ) ) ;
#9529=DIRECTION ( 'NONE',  ( 0.000000000000000000, 0.4999999999999996669, 0.8660254037844388186 ) ) ;
#9533=CARTESIAN_POINT ( 'NONE',  ( 1.560000000000005826, -1.732050807568885631, 0.000000000000000000 ) ) ;
#9579=EDGE_LOOP ( 'NONE', ( #14146, #1003, #12891 ) ) ;
#9593=AXIS2_PLACEMENT_3D ( 'NONE', #2465, #6914, #6029 ) ;
#9617=ORIENTED_EDGE ( 'NONE', *, *, #13491, .F. ) ;
#9626=ORIENTED_EDGE ( 'NONE', *, *, #4591, .T. ) ;
#9633=DIRECTION ( 'NONE',  ( 0.000000000000000000, 0.4999999999999997780, -0.8660254037844387076 ) ) ;
#9645=AXIS2_PLACEMENT_3D ( 'NONE', #10796, #7479, #5235 ) ;
#9664=EDGE_LOOP ( 'NONE', ( #4653, #1799, #2012 ) ) ;
#9707=ORIENTED_EDGE ( 'NONE', *, *, #12835, .T. ) ;
#9709=PLANE ( 'NONE',  #3026 ) ;
#9717=ORIENTED_EDGE ( 'NONE', *, *, #125, .F. ) ;
#9720=EDGE_LOOP ( 'NONE', ( #2810, #6882 ) ) ;
#9727=CARTESIAN_POINT ( 'NONE',  ( 2.750000000000002665, 0.000000000000000000, 0.000000000000000000 ) ) ;
#9824=FACE_OUTER_BOUND ( 'NONE', #13372, .T. ) ;
#9856=FACE_OUTER_BOUND ( 'NONE', #12614, .T. ) ;
#9882=EDGE_CURVE ( 'NONE', #2918, #11701, #1690, .T. ) ;
#9891=CARTESIAN_POINT ( 'NONE',  ( 0.000000000000000000, 0.8660254037844428154, -1.500000000000001332 ) ) ;
#9898=VECTOR ( 'NONE', #2936, 1000.000000000000000 ) ;
#9911=ORIENTED_EDGE ( 'NONE', *, *, #8315, .T. ) ;
#9923=CARTESIAN_POINT ( 'NONE',  ( 1.560000000000005826, 0.8660254037844428154, 1.500000000000001332 ) ) ;
#9938=LINE ( 'NONE', #5327, #10699 ) ;
#9958=DIRECTION ( 'NONE',  ( 0.000000000000000000, 0.000000000000000000, -1.000000000000000000 ) ) ;
#9962=ORIENTED_EDGE ( 'NONE', *, *, #12092, .T. ) ;
#9966=DIRECTION ( 'NONE',  ( 0.000000000000000000, 0.000000000000000000, 1.000000000000000000 ) ) ;
#10028=ADVANCED_FACE ( 'NONE', ( #9824 ), #14099, .T. ) ;
#10039=CARTESIAN_POINT ( 'NONE',  ( 1.560000000000005826, 0.8660254037844428154, 1.500000000000001332 ) ) ;
#10079=( GEOMETRIC_REPRESENTATION_CONTEXT ( 3 ) GLOBAL_UNCERTAINTY_ASSIGNED_CONTEXT ( ( #5141 ) ) GLOBAL_UNIT_ASSIGNED_CONTEXT ( ( #4992, #13781, #9452 ) ) REPRESENTATION_CONTEXT ( 'NONE', 'WORKASPACE' ) );
#10119=VECTOR ( 'NONE', #7397, 1000.000000000000114 ) ;
#10139=ORIENTED_EDGE ( 'NONE', *, *, #14050, .T. ) ;
#10169=CARTESIAN_POINT ( 'NONE',  ( 2.949999999999994404, 0.000000000000000000, 2.699999999999999289 ) ) ;
#10174=EDGE_CURVE ( 'NONE', #6239, #13071, #9150, .T. ) ;
#10216=EDGE_LOOP ( 'NONE', ( #8636, #9911, #143, #6010, #9090 ) ) ;
#10238=CARTESIAN_POINT ( 'NONE',  ( 27.30499999999998195, 0.000000000000000000, 0.000000000000000000 ) ) ;
#10242=AXIS2_PLACEMENT_3D ( 'NONE', #4012, #11601, #1810 ) ;
#10251=CARTESIAN_POINT ( 'NONE',  ( 1.560000000000005826, -1.732050807568885631, 0.000000000000000000 ) ) ;
#10349=CARTESIAN_POINT ( 'NONE',  ( 0.000000000000000000, -0.8660254037844428154, -1.500000000000001332 ) ) ;
#10360=VECTOR ( 'NONE', #4780, 1000.000000000000114 ) ;
#10401=EDGE_LOOP ( 'NONE', ( #267, #5711, #6219 ) ) ;
#10412=DIRECTION ( 'NONE',  ( 0.000000000000000000, 0.000000000000000000, -1.000000000000000000 ) ) ;
#10413=DIRECTION ( 'NONE',  ( -1.000000000000000000, 0.000000000000000000, 0.000000000000000000 ) ) ;
#10417=FACE_OUTER_BOUND ( 'NONE', #8036, .T. ) ;
#10429=ORIENTED_EDGE ( 'NONE', *, *, #14344, .T. ) ;
#10432=CARTESIAN_POINT ( 'NONE',  ( 27.75000000000001066, 0.000000000000000000, 2.055000000000000160 ) ) ;
#10452=AXIS2_PLACEMENT_3D ( 'NONE', #2387, #7796, #13453 ) ;
#10453=DIRECTION ( 'NONE',  ( 0.000000000000000000, 1.000000000000000000, 0.000000000000000000 ) ) ;
#10469=ADVANCED_BREP_SHAPE_REPRESENTATION ( '', ( #11914, #11025 ), #10079 ) ;
#10481=ADVANCED_FACE ( 'NONE', ( #11322 ), #202, .F. ) ;
#10488=DIRECTION ( 'NONE',  ( 0.000000000000000000, 0.000000000000000000, 1.000000000000000000 ) ) ;
#10545=AXIS2_PLACEMENT_3D ( 'NONE', #5838, #3748, #11414 ) ;
#10551=VERTEX_POINT ( 'NONE', #653 ) ;
#10553=DIRECTION ( 'NONE',  ( -0.000000000000000000, -0.5000000000000011102, -0.8660254037844379305 ) ) ;
#10554=EDGE_LOOP ( 'NONE', ( #8119, #6390, #4948, #3119 ) ) ;
#10572=AXIS2_PLACEMENT_3D ( 'NONE', #13921, #10833, #7319 ) ;
#10591=EDGE_CURVE ( 'NONE', #2918, #658, #4925, .T. ) ;
#10596=CARTESIAN_POINT ( 'NONE',  ( 1.560000000000005826, -1.732050807568885631, 0.000000000000000000 ) ) ;
#10632=APPLICATION_CONTEXT ( 'automotive_design' ) ;
#10648=( NAMED_UNIT ( * ) SI_UNIT ( $, .STERADIAN. ) SOLID_ANGLE_UNIT ( ) );
#10658=DIRECTION ( 'NONE',  ( 0.000000000000000000, 0.000000000000000000, 1.000000000000000000 ) ) ;
#10672=EDGE_CURVE ( 'NONE', #658, #10551, #12878, .T. ) ;
#10673=EDGE_CURVE ( 'NONE', #6239, #11431, #5386, .T. ) ;
#10678=EDGE_CURVE ( 'NONE', #1861, #11793, #6722, .T. ) ;
#10682=CARTESIAN_POINT ( 'NONE',  ( 4.755015822784813828, 0.000000000000000000, 0.000000000000000000 ) ) ;
#10699=VECTOR ( 'NONE', #8695, 1000.000000000000114 ) ;
#10760=EDGE_CURVE ( 'NONE', #3285, #1341, #7596, .T. ) ;
#10767=DIRECTION ( 'NONE',  ( -1.000000000000000000, 0.000000000000000000, 0.000000000000000000 ) ) ;
#10787=EDGE_LOOP ( 'NONE', ( #5836, #1728, #14049, #1822, #1305 ) ) ;
#10789=CARTESIAN_POINT ( 'NONE',  ( 4.755015822784813828, 0.000000000000000000, 0.000000000000000000 ) ) ;
#10796=CARTESIAN_POINT ( 'NONE',  ( 0.000000000000000000, 0.000000000000000000, 0.000000000000000000 ) ) ;
#10827=DIRECTION ( 'NONE',  ( 0.000000000000000000, 0.000000000000000000, 1.000000000000000000 ) ) ;
#10833=DIRECTION ( 'NONE',  ( -1.000000000000000000, 0.000000000000000000, 0.000000000000000000 ) ) ;
#10853=CARTESIAN_POINT ( 'NONE',  ( 4.755015822784813828, 0.000000000000000000, 0.000000000000000000 ) ) ;
#10856=DIRECTION ( 'NONE',  ( 0.000000000000000000, 0.000000000000000000, -1.000000000000000000 ) ) ;
#10859=DIRECTION ( 'NONE',  ( 0.000000000000000000, 0.000000000000000000, 1.000000000000000000 ) ) ;
#10863=LINE ( 'NONE', #14173, #3462 ) ;
#10896=FACE_OUTER_BOUND ( 'NONE', #3925, .T. ) ;
#10909=AXIS2_PLACEMENT_3D ( 'NONE', #2180, #13302, #4594 ) ;
#10916=CARTESIAN_POINT ( 'NONE',  ( 1.560000000000005826, -0.8660254037844428154, -1.500000000000001332 ) ) ;
#10919=AXIS2_PLACEMENT_3D ( 'NONE', #4318, #14328, #916 ) ;
#10934=DIRECTION ( 'NONE',  ( -0.000000000000000000, -0.5000000000000011102, -0.8660254037844379305 ) ) ;
#10960=PLANE ( 'NONE',  #9138 ) ;
#10989=AXIS2_PLACEMENT_3D ( 'NONE', #4415, #946, #14358 ) ;
#11012=CARTESIAN_POINT ( 'NONE',  ( 2.369999999999996998, 0.000000000000000000, 4.750000000000000000 ) ) ;
#11025=AXIS2_PLACEMENT_3D ( 'NONE', #167, #6524, #5441 ) ;
#11051=CARTESIAN_POINT ( 'NONE',  ( 2.949999999999994404, 3.306546357697852747E-16, -2.699999999999999289 ) ) ;
#11070=CARTESIAN_POINT ( 'NONE',  ( 1.560000000000005826, 0.000000000000000000, 1.500000000000001332 ) ) ;
#11103=FACE_OUTER_BOUND ( 'NONE', #9579, .T. ) ;
#11143=EDGE_CURVE ( 'NONE', #11793, #7871, #9132, .T. ) ;
#11147=ORIENTED_EDGE ( 'NONE', *, *, #10672, .F. ) ;
#11184=ORIENTED_EDGE ( 'NONE', *, *, #6368, .F. ) ;
#11191=CARTESIAN_POINT ( 'NONE',  ( 27.75000000000001066, 2.789133085058096608E-16, -2.055000000000000160 ) ) ;
#11194=ORIENTED_EDGE ( 'NONE', *, *, #6140, .T. ) ;
#11225=CIRCLE ( 'NONE', #3295, 5.315148208181398104 ) ;
#11261=DIRECTION ( 'NONE',  ( -0.5000000000000042188, 1.060575238724903710E-16, -0.8660254037844361541 ) ) ;
#11279=ORIENTED_EDGE ( 'NONE', *, *, #8811, .T. ) ;
#11301=PLANE ( 'NONE',  #6784 ) ;
#11313=EDGE_CURVE ( 'NONE', #375, #3412, #7275, .T. ) ;
#11322=FACE_OUTER_BOUND ( 'NONE', #10401, .T. ) ;
#11352=ADVANCED_FACE ( 'NONE', ( #11785 ), #5265, .T. ) ;
#11357=ADVANCED_FACE ( 'NONE', ( #11103 ), #10960, .F. ) ;
#11373=DIRECTION ( 'NONE',  ( 0.000000000000000000, 0.000000000000000000, 1.000000000000000000 ) ) ;
#11375=ORIENTED_EDGE ( 'NONE', *, *, #14183, .F. ) ;
#11390=DIRECTION ( 'NONE',  ( 0.000000000000000000, 0.000000000000000000, 1.000000000000000000 ) ) ;
#11414=DIRECTION ( 'NONE',  ( 0.000000000000000000, 0.000000000000000000, 1.000000000000000000 ) ) ;
#11431=VERTEX_POINT ( 'NONE', #13399 ) ;
#11442=CARTESIAN_POINT ( 'NONE',  ( 1.560000000000005826, 0.8660254037844428154, -1.500000000000001332 ) ) ;
#11452=CARTESIAN_POINT ( 'NONE',  ( 1.560000000000005826, -1.299038105676664223, 0.7500000000000006661 ) ) ;
#11453=ORIENTED_EDGE ( 'NONE', *, *, #5923, .T. ) ;
#11456=CARTESIAN_POINT ( 'NONE',  ( -997.5739745962155212, 0.000000000000000000, 0.000000000000000000 ) ) ;
#11518=LINE ( 'NONE', #11442, #8463 ) ;
#11519=ORIENTED_EDGE ( 'NONE', *, *, #9028, .T. ) ;
#11527=VERTEX_POINT ( 'NONE', #12625 ) ;
#11579=CARTESIAN_POINT ( 'NONE',  ( 27.75000000000001066, 0.000000000000000000, 0.000000000000000000 ) ) ;
#11585=SURFACE_SIDE_STYLE ('',( #2749 ) ) ;
#11590=DIRECTION ( 'NONE',  ( 0.000000000000000000, 1.000000000000000000, 0.000000000000000000 ) ) ;
#11592=ORIENTED_EDGE ( 'NONE', *, *, #10673, .F. ) ;
#11596=CIRCLE ( 'NONE', #12312, 1.500000000000000000 ) ;
#11601=DIRECTION ( 'NONE',  ( -1.000000000000000000, 0.000000000000000000, 0.000000000000000000 ) ) ;
#11615=ORIENTED_EDGE ( 'NONE', *, *, #14183, .T. ) ;
#11639=SHAPE_REPRESENTATION_RELATIONSHIP ( 'NONE' , 'NONE' ,  #3865, #10469 ) ;
#11691=CARTESIAN_POINT ( 'NONE',  ( 1.560000000000005826, 0.8660254037844428154, 1.500000000000001332 ) ) ;
#11701=VERTEX_POINT ( 'NONE', #11012 ) ;
#11705=DIRECTION ( 'NONE',  ( -1.000000000000000000, 0.000000000000000000, 0.000000000000000000 ) ) ;
#11718=CARTESIAN_POINT ( 'NONE',  ( 1.560000000000005826, -1.732050807568885631, 0.000000000000000000 ) ) ;
#11719=DIRECTION ( 'NONE',  ( 0.000000000000000000, 0.000000000000000000, 1.000000000000000000 ) ) ;
#11725=LINE ( 'NONE', #5058, #12566 ) ;
#11735=CARTESIAN_POINT ( 'NONE',  ( 1.560000000000005826, 0.8660254037844428154, -1.500000000000001332 ) ) ;
#11748=CIRCLE ( 'NONE', #2175, 4.750000000000000000 ) ;
#11754=EDGE_CURVE ( 'NONE', #8562, #5249, #6760, .T. ) ;
#11758=FACE_OUTER_BOUND ( 'NONE', #10554, .T. ) ;
#11785=FACE_OUTER_BOUND ( 'NONE', #10216, .T. ) ;
#11793=VERTEX_POINT ( 'NONE', #10349 ) ;
#11809=CARTESIAN_POINT ( 'NONE',  ( 1.560000000000005826, 1.299038105676664223, -0.7500000000000006661 ) ) ;
#11814=CARTESIAN_POINT ( 'NONE',  ( 0.000000000000000000, 1.732050807568871864, 0.000000000000000000 ) ) ;
#11818=CIRCLE ( 'NONE', #9300, 4.750000000000000000 ) ;
#11831=DIRECTION ( 'NONE',  ( 0.000000000000000000, 0.000000000000000000, 1.000000000000000000 ) ) ;
#11841=ADVANCED_FACE ( 'NONE', ( #10417 ), #3544, .F. ) ;
#11855=DIRECTION ( 'NONE',  ( 0.000000000000000000, 0.000000000000000000, -1.000000000000000000 ) ) ;
#11887=ORIENTED_EDGE ( 'NONE', *, *, #1310, .F. ) ;
#11911=DIRECTION ( 'NONE',  ( 0.000000000000000000, 0.000000000000000000, -1.000000000000000000 ) ) ;
#11914=MANIFOLD_SOLID_BREP ( 'Hex', #12488 ) ;
#11984=LINE ( 'NONE', #1961, #2060 ) ;
#12020=TOROIDAL_SURFACE ( 'NONE', #5001, 2.699999999999999289, 0.2000000000000000111 ) ;
#12022=EDGE_CURVE ( 'NONE', #5483, #11527, #13143, .T. ) ;
#12030=PLANE ( 'NONE',  #374 ) ;
#12055=CYLINDRICAL_SURFACE ( 'NONE', #10919, 4.750000000000000000 ) ;
#12060=ORIENTED_EDGE ( 'NONE', *, *, #5890, .F. ) ;
#12068=CYLINDRICAL_SURFACE ( 'NONE', #2291, 2.499999999999999112 ) ;
#12069=DIRECTION ( 'NONE',  ( 0.000000000000000000, 1.000000000000000000, 0.000000000000000000 ) ) ;
#12079=DIRECTION ( 'NONE',  ( 1.000000000000000000, 0.000000000000000000, 0.000000000000000000 ) ) ;
#12092=EDGE_CURVE ( 'NONE', #13268, #6118, #3455, .T. ) ;
#12144=ORIENTED_EDGE ( 'NONE', *, *, #12783, .F. ) ;
#12153=VECTOR ( 'NONE', #4539, 1000.000000000000000 ) ;
#12160=DIRECTION ( 'NONE',  ( -1.000000000000000000, 0.000000000000000000, 0.000000000000000000 ) ) ;
#12171=STYLED_ITEM ( 'NONE', ( #8287 ), #11914 ) ;
#12205=DIRECTION ( 'NONE',  ( 0.000000000000000000, 0.000000000000000000, 1.000000000000000000 ) ) ;
#12239=LINE ( 'NONE', #4428, #6122 ) ;
#12273=ORIENTED_EDGE ( 'NONE', *, *, #1101, .F. ) ;
#12277=LINE ( 'NONE', #61, #12153 ) ;
#12289=PLANE ( 'NONE',  #1473 ) ;
#12290=EDGE_LOOP ( 'NONE', ( #5744, #7404, #6906, #2017, #4167, #4063 ) ) ;
#12312=AXIS2_PLACEMENT_3D ( 'NONE', #7466, #6165, #823 ) ;
#12328=ORIENTED_EDGE ( 'NONE', *, *, #5100, .T. ) ;
#12337=VERTEX_POINT ( 'NONE', #5050 ) ;
#12374=DIRECTION ( 'NONE',  ( -1.000000000000000000, 0.000000000000000000, 0.000000000000000000 ) ) ;
#12377=CARTESIAN_POINT ( 'NONE',  ( 2.750000000000002665, 2.500000000000002220, 0.000000000000000000 ) ) ;
#12404=VECTOR ( 'NONE', #6593, 1000.000000000000000 ) ;
#12423=DIRECTION ( 'NONE',  ( 0.000000000000000000, 0.000000000000000000, 1.000000000000000000 ) ) ;
#12488=CLOSED_SHELL ( 'NONE', ( #2437, #702, #14077, #9003, #7116, #11352, #1765, #10028, #13693, #13118, #14334, #5592, #5116, #11841, #5805, #13473, #5708, #4009, #2662, #8309, #4433, #6000, #8825, #11357, #8338, #10481, #6289 ) ) ;
#12546=CIRCLE ( 'NONE', #10909, 4.750000000000000000 ) ;
#12566=VECTOR ( 'NONE', #9529, 1000.000000000000114 ) ;
#12595=DIRECTION ( 'NONE',  ( 0.000000000000000000, 1.000000000000000000, 0.000000000000000000 ) ) ;
#12599=DIRECTION ( 'NONE',  ( -1.000000000000000000, 0.000000000000000000, 0.000000000000000000 ) ) ;
#12608=FACE_OUTER_BOUND ( 'NONE', #4372, .T. ) ;
#12614=EDGE_LOOP ( 'NONE', ( #12745, #8288, #14420, #13514, #13056 ) ) ;
#12616=ORIENTED_EDGE ( 'NONE', *, *, #11754, .T. ) ;
#12620=EDGE_CURVE ( 'NONE', #13071, #12337, #5185, .T. ) ;
#12625=CARTESIAN_POINT ( 'NONE',  ( 27.30499999999998195, 3.061616997868382648E-16, -2.499999999999999556 ) ) ;
#12633=EDGE_LOOP ( 'NONE', ( #9717, #8349, #4195, #11453, #1841 ) ) ;
#12697=VERTEX_POINT ( 'NONE', #11191 ) ;
#12703=FACE_OUTER_BOUND ( 'NONE', #5658, .T. ) ;
#12740=EDGE_LOOP ( 'NONE', ( #2661, #12328, #3605, #3758, #6272 ) ) ;
#12745=ORIENTED_EDGE ( 'NONE', *, *, #10760, .T. ) ;
#12783=EDGE_CURVE ( 'NONE', #5483, #12337, #2733, .T. ) ;
#12789=EDGE_CURVE ( 'NONE', #3412, #14130, #7168, .T. ) ;
#12792=EDGE_LOOP ( 'NONE', ( #7984, #5727, #7590, #12873, #12273 ) ) ;
#12818=AXIS2_PLACEMENT_3D ( 'NONE', #8754, #52, #7935 ) ;
#12822=AXIS2_PLACEMENT_3D ( 'NONE', #11456, #3504, #5885 ) ;
#12835=EDGE_CURVE ( 'NONE', #11527, #11431, #4709, .T. ) ;
#12837=CARTESIAN_POINT ( 'NONE',  ( 2.750000000000002665, 0.000000000000000000, 0.000000000000000000 ) ) ;
#12873=ORIENTED_EDGE ( 'NONE', *, *, #824, .F. ) ;
#12878=CIRCLE ( 'NONE', #10989, 2.375000000000000000 ) ;
#12891=ORIENTED_EDGE ( 'NONE', *, *, #4108, .F. ) ;
#13017=DIRECTION ( 'NONE',  ( 0.000000000000000000, -0.4999999999999997224, 0.8660254037844387076 ) ) ;
#13023=EDGE_CURVE ( 'NONE', #12697, #11527, #12239, .T. ) ;
#13037=SHAPE_DEFINITION_REPRESENTATION ( #1467, #3865 ) ;
#13048=EDGE_CURVE ( 'NONE', #2724, #3412, #5423, .T. ) ;
#13056=ORIENTED_EDGE ( 'NONE', *, *, #283, .F. ) ;
#13062=VECTOR ( 'NONE', #5281, 1000.000000000000000 ) ;
#13071=VERTEX_POINT ( 'NONE', #8787 ) ;
#13076=CARTESIAN_POINT ( 'NONE',  ( 1.560000000000005826, 1.732050807568871864, 0.000000000000000000 ) ) ;
#13078=VECTOR ( 'NONE', #3447, 1000.000000000000114 ) ;
#13100=ORIENTED_EDGE ( 'NONE', *, *, #11143, .F. ) ;
#13118=ADVANCED_FACE ( 'NONE', ( #6734, #7906 ), #955, .F. ) ;
#13143=CIRCLE ( 'NONE', #7497, 2.499999999999999556 ) ;
#13154=AXIS2_PLACEMENT_3D ( 'NONE', #10789, #10856, #769 ) ;
#13213=VERTEX_POINT ( 'NONE', #3529 ) ;
#13262=CARTESIAN_POINT ( 'NONE',  ( 1.560000000000005826, -1.732050807568885631, 0.000000000000000000 ) ) ;
#13268=VERTEX_POINT ( 'NONE', #6881 ) ;
#13302=DIRECTION ( 'NONE',  ( -1.000000000000000000, 0.000000000000000000, 0.000000000000000000 ) ) ;
#13312=CARTESIAN_POINT ( 'NONE',  ( 0.000000000000000000, 0.000000000000000000, 0.000000000000000000 ) ) ;
#13319=LINE ( 'NONE', #5612, #2892 ) ;
#13332=DIRECTION ( 'NONE',  ( 0.000000000000000000, -1.224646799147353207E-16, 1.000000000000000000 ) ) ;
#13347=EDGE_CURVE ( 'NONE', #1341, #4098, #1450, .T. ) ;
#13360=CARTESIAN_POINT ( 'NONE',  ( 2.750000000000002665, 0.000000000000000000, 0.000000000000000000 ) ) ;
#13372=EDGE_LOOP ( 'NONE', ( #3023, #5198, #9626, #11194, #11147 ) ) ;
#13399=CARTESIAN_POINT ( 'NONE',  ( 2.949999999999994404, 3.061616997868382155E-16, -2.499999999999999112 ) ) ;
#13443=DIRECTION ( 'NONE',  ( -1.000000000000000000, 0.000000000000000000, 0.000000000000000000 ) ) ;
#13453=DIRECTION ( 'NONE',  ( 0.000000000000000000, 0.000000000000000000, -1.000000000000000000 ) ) ;
#13473=ADVANCED_FACE ( 'NONE', ( #10896 ), #12289, .T. ) ;
#13491=EDGE_CURVE ( 'NONE', #5215, #1341, #13319, .T. ) ;
#13493=CARTESIAN_POINT ( 'NONE',  ( 1.560000000000005826, -0.8660254037844428154, 1.500000000000001332 ) ) ;
#13505=PRODUCT ( 'socket button head screw_iso_ISO 7380 - M5 x 25 - 25N', 'socket button head screw_iso_ISO 7380 - M5 x 25 - 25N', '', ( #14137 ) ) ;
#13514=ORIENTED_EDGE ( 'NONE', *, *, #5650, .F. ) ;
#13523=ORIENTED_EDGE ( 'NONE', *, *, #8473, .T. ) ;
#13531=DIRECTION ( 'NONE',  ( -1.000000000000000000, 0.000000000000000000, 0.000000000000000000 ) ) ;
#13601=EDGE_CURVE ( 'NONE', #10551, #658, #5657, .T. ) ;
#13693=ADVANCED_FACE ( 'NONE', ( #4001 ), #1872, .T. ) ;
#13719=LINE ( 'NONE', #6960, #8894 ) ;
#13730=DIRECTION ( 'NONE',  ( -1.000000000000000000, 0.000000000000000000, 0.000000000000000000 ) ) ;
#13781=( NAMED_UNIT ( * ) PLANE_ANGLE_UNIT ( ) SI_UNIT ( $, .RADIAN. ) );
#13806=CYLINDRICAL_SURFACE ( 'NONE', #86, 2.499999999999999112 ) ;
#13844=CARTESIAN_POINT ( 'NONE',  ( 0.000000000000000000, 0.8660254037844428154, -1.500000000000001332 ) ) ;
#13858=PRODUCT_DEFINITION ( 'UNKNOWN', '', #5678, #5834 ) ;
#13860=FILL_AREA_STYLE_COLOUR ( '', #2153 ) ;
#13908=ORIENTED_EDGE ( 'NONE', *, *, #6368, .T. ) ;
#13921=CARTESIAN_POINT ( 'NONE',  ( 1.560000000000005826, 0.000000000000000000, 0.000000000000000000 ) ) ;
#13976=ORIENTED_EDGE ( 'NONE', *, *, #10174, .T. ) ;
#13983=CIRCLE ( 'NONE', #3930, 4.750000000000000000 ) ;
#13993=EDGE_CURVE ( 'NONE', #4098, #3285, #6071, .T. ) ;
#14012=DIRECTION ( 'NONE',  ( 0.000000000000000000, 0.000000000000000000, 1.000000000000000000 ) ) ;
#14020=CARTESIAN_POINT ( 'NONE',  ( 2.426025403784448642, 0.000000000000000000, 0.000000000000000000 ) ) ;
#14035=ORIENTED_EDGE ( 'NONE', *, *, #5923, .F. ) ;
#14049=ORIENTED_EDGE ( 'NONE', *, *, #283, .T. ) ;
#14050=EDGE_CURVE ( 'NONE', #1181, #8562, #5137, .T. ) ;
#14064=MECHANICAL_DESIGN_GEOMETRIC_PRESENTATION_REPRESENTATION('',(#12171),#5402);
#14077=ADVANCED_FACE ( 'NONE', ( #819 ), #3137, .T. ) ;
#14092=DIRECTION ( 'NONE',  ( 0.000000000000000000, -0.4999999999999996114, -0.8660254037844388186 ) ) ;
#14099=SPHERICAL_SURFACE ( 'NONE', #13154, 5.315148208181398104 ) ;
#14122=AXIS2_PLACEMENT_3D ( 'NONE', #6301, #3108, #14012 ) ;
#14130=VERTEX_POINT ( 'NONE', #9533 ) ;
#14137=PRODUCT_CONTEXT ( 'NONE', #4579, 'mechanical' ) ;
#14146=ORIENTED_EDGE ( 'NONE', *, *, #3180, .F. ) ;
#14161=DIRECTION ( 'NONE',  ( 1.000000000000000000, 0.000000000000000000, 0.000000000000000000 ) ) ;
#14173=CARTESIAN_POINT ( 'NONE',  ( 1.560000000000005826, 1.732050807568871864, 0.000000000000000000 ) ) ;
#14183=EDGE_CURVE ( 'NONE', #11527, #5483, #1482, .T. ) ;
#14243=EDGE_LOOP ( 'NONE', ( #7022, #13976 ) ) ;
#14250=FACE_OUTER_BOUND ( 'NONE', #10787, .T. ) ;
#14275=CARTESIAN_POINT ( 'NONE',  ( 1.560000000000005826, -0.8660254037844428154, -1.500000000000001332 ) ) ;
#14281=CONICAL_SURFACE ( 'NONE', #1653, 1732.050807568857181, 1.047197551196592746 ) ;
#14290=AXIS2_PLACEMENT_3D ( 'NONE', #2850, #7295, #421 ) ;
#14300=VECTOR ( 'NONE', #10453, 1000.000000000000000 ) ;
#14313=VECTOR ( 'NONE', #5995, 1000.000000000000000 ) ;
#14328=DIRECTION ( 'NONE',  ( -1.000000000000000000, 0.000000000000000000, 0.000000000000000000 ) ) ;
#14334=ADVANCED_FACE ( 'NONE', ( #12608 ), #13806, .T. ) ;
#14335=CARTESIAN_POINT ( 'NONE',  ( 1.560000000000005826, -1.299038105676650456, -0.7500000000000006661 ) ) ;
#14344=EDGE_CURVE ( 'NONE', #2567, #12697, #4757, .T. ) ;
#14358=DIRECTION ( 'NONE',  ( 0.000000000000000000, 0.000000000000000000, 1.000000000000000000 ) ) ;
#14383=EDGE_CURVE ( 'NONE', #1326, #7871, #11518, .T. ) ;
#14401=FACE_OUTER_BOUND ( 'NONE', #9664, .T. ) ;
#14420=ORIENTED_EDGE ( 'NONE', *, *, #1101, .T. ) ;
#14437=DIRECTION ( 'NONE',  ( -0.7071067811865513475, 8.659560562354886020E-17, -0.7071067811865436870 ) ) ;
#14438=CARTESIAN_POINT ( 'NONE',  ( 27.30499999999998195, 0.000000000000000000, 0.000000000000000000 ) ) ;
#14441=LINE ( 'NONE', #13493, #2250 ) ;
#14447=CIRCLE ( 'NONE', #8592, 1.500000000000000000 ) ;
ENDSEC;
END-ISO-10303-21;
